ISO-10303-21;
HEADER;
/* Generated by software containing ST-Developer
 * from STEP Tools, Inc. (www.steptools.com) 
 */

FILE_DESCRIPTION(
/* description */ ('Bell-crank linkage with push rods'),
/* implementation_level */ '2;1');

FILE_NAME(
/* name */ 'Pin keeper (1).step',
/* time_stamp */ '2026-10-28T03:25:15-07:00',
/* author */ (''),
/* organization */ (''),
/* preprocessor_version */ 'ST-DEVELOPER v20.2',
/* originating_system */ 'Autodesk Translation Framework v15.17.0.0',
/* authorisation */ '');

FILE_SCHEMA (('AUTOMOTIVE_DESIGN { 1 0 10303 214 3 1 1 }'));
ENDSEC;

DATA;
#10=MECHANICAL_DESIGN_GEOMETRIC_PRESENTATION_REPRESENTATION('',(#640),#16678);
#524=SHAPE_REPRESENTATION_RELATIONSHIP('SRR','None',#16942,#578);
#578=ADVANCED_BREP_SHAPE_REPRESENTATION('',(#701),#16647);
#640=STYLED_ITEM('',(#17291),#701);
#701=MANIFOLD_SOLID_BREP('Body1',#8831);
#854=FACE_BOUND('',#2206,.T.);
#855=FACE_BOUND('',#2208,.T.);
#1121=PLANE('',#10113);
#1122=PLANE('',#10114);
#1552=FACE_OUTER_BOUND('',#2203,.T.);
#1553=FACE_OUTER_BOUND('',#2204,.T.);
#1554=FACE_OUTER_BOUND('',#2205,.T.);
#1555=FACE_OUTER_BOUND('',#2207,.T.);
#2203=EDGE_LOOP('',(#7213,#7214,#7215,#7216));
#2204=EDGE_LOOP('',(#7217,#7218,#7219,#7220));
#2205=EDGE_LOOP('',(#7221));
#2206=EDGE_LOOP('',(#7222));
#2207=EDGE_LOOP('',(#7223));
#2208=EDGE_LOOP('',(#7224));
#2834=LINE('',#15503,#3383);
#2835=LINE('',#15509,#3384);
#3383=VECTOR('',#12242,0.225);
#3384=VECTOR('',#12249,0.5);
#3940=CIRCLE('',#10108,0.225);
#3941=CIRCLE('',#10109,0.225);
#3942=CIRCLE('',#10111,0.5);
#3943=CIRCLE('',#10112,0.5);
#4551=VERTEX_POINT('',#15500);
#4552=VERTEX_POINT('',#15502);
#4553=VERTEX_POINT('',#15506);
#4554=VERTEX_POINT('',#15508);
#5484=EDGE_CURVE('',#4551,#4551,#3940,.T.);
#5485=EDGE_CURVE('',#4551,#4552,#2834,.T.);
#5486=EDGE_CURVE('',#4552,#4552,#3941,.T.);
#5487=EDGE_CURVE('',#4553,#4553,#3942,.T.);
#5488=EDGE_CURVE('',#4553,#4554,#2835,.T.);
#5489=EDGE_CURVE('',#4554,#4554,#3943,.T.);
#7213=ORIENTED_EDGE('',*,*,#5484,.F.);
#7214=ORIENTED_EDGE('',*,*,#5485,.T.);
#7215=ORIENTED_EDGE('',*,*,#5486,.T.);
#7216=ORIENTED_EDGE('',*,*,#5485,.F.);
#7217=ORIENTED_EDGE('',*,*,#5487,.F.);
#7218=ORIENTED_EDGE('',*,*,#5488,.T.);
#7219=ORIENTED_EDGE('',*,*,#5489,.T.);
#7220=ORIENTED_EDGE('',*,*,#5488,.F.);
#7221=ORIENTED_EDGE('',*,*,#5487,.T.);
#7222=ORIENTED_EDGE('',*,*,#5484,.T.);
#7223=ORIENTED_EDGE('',*,*,#5489,.F.);
#7224=ORIENTED_EDGE('',*,*,#5486,.F.);
#8189=CYLINDRICAL_SURFACE('',#10107,0.225);
#8190=CYLINDRICAL_SURFACE('',#10110,0.5);
#8577=ADVANCED_FACE('',(#1552),#8189,.F.);
#8578=ADVANCED_FACE('',(#1553),#8190,.T.);
#8579=ADVANCED_FACE('',(#1554,#854),#1121,.T.);
#8580=ADVANCED_FACE('',(#1555,#855),#1122,.F.);
#8831=CLOSED_SHELL('',(#8577,#8578,#8579,#8580));
#10106=AXIS2_PLACEMENT_3D('',#15498,#12236,#12237);
#10107=AXIS2_PLACEMENT_3D('',#15499,#12238,#12239);
#10108=AXIS2_PLACEMENT_3D('',#15501,#12240,#12241);
#10109=AXIS2_PLACEMENT_3D('',#15504,#12243,#12244);
#10110=AXIS2_PLACEMENT_3D('',#15505,#12245,#12246);
#10111=AXIS2_PLACEMENT_3D('',#15507,#12247,#12248);
#10112=AXIS2_PLACEMENT_3D('',#15510,#12250,#12251);
#10113=AXIS2_PLACEMENT_3D('',#15511,#12252,#12253);
#10114=AXIS2_PLACEMENT_3D('',#15512,#12254,#12255);
#12236=DIRECTION('axis',(0.,0.,1.));
#12237=DIRECTION('refdir',(1.,0.,0.));
#12238=DIRECTION('center_axis',(0.,0.,1.));
#12239=DIRECTION('ref_axis',(1.,0.,0.));
#12240=DIRECTION('center_axis',(0.,0.,-1.));
#12241=DIRECTION('ref_axis',(1.,0.,0.));
#12242=DIRECTION('',(0.,0.,-1.));
#12243=DIRECTION('center_axis',(0.,0.,-1.));
#12244=DIRECTION('ref_axis',(1.,0.,0.));
#12245=DIRECTION('center_axis',(0.,0.,1.));
#12246=DIRECTION('ref_axis',(1.,0.,0.));
#12247=DIRECTION('center_axis',(0.,0.,1.));
#12248=DIRECTION('ref_axis',(1.,0.,0.));
#12249=DIRECTION('',(0.,0.,-1.));
#12250=DIRECTION('center_axis',(0.,0.,1.));
#12251=DIRECTION('ref_axis',(1.,0.,0.));
#12252=DIRECTION('center_axis',(0.,0.,1.));
#12253=DIRECTION('ref_axis',(1.,0.,0.));
#12254=DIRECTION('center_axis',(0.,0.,1.));
#12255=DIRECTION('ref_axis',(1.,0.,0.));
#15498=CARTESIAN_POINT('',(0.,0.,0.));
#15499=CARTESIAN_POINT('Origin',(4.,0.,8.1));
#15500=CARTESIAN_POINT('',(3.775,-2.75545529808154E-17,8.3));
#15501=CARTESIAN_POINT('Origin',(4.,0.,8.3));
#15502=CARTESIAN_POINT('',(3.775,-2.75545529808154E-17,8.1));
#15503=CARTESIAN_POINT('',(3.775,-2.75545529808154E-17,8.1));
#15504=CARTESIAN_POINT('Origin',(4.,0.,8.1));
#15505=CARTESIAN_POINT('Origin',(4.,0.,8.1));
#15506=CARTESIAN_POINT('',(3.5,-6.12323399573677E-17,8.3));
#15507=CARTESIAN_POINT('Origin',(4.,0.,8.3));
#15508=CARTESIAN_POINT('',(3.5,-6.12323399573677E-17,8.1));
#15509=CARTESIAN_POINT('',(3.5,-6.12323399573677E-17,8.1));
#15510=CARTESIAN_POINT('Origin',(4.,0.,8.1));
#15511=CARTESIAN_POINT('Origin',(4.,0.,8.3));
#15512=CARTESIAN_POINT('Origin',(4.,0.,8.1));
#16583=UNCERTAINTY_MEASURE_WITH_UNIT(LENGTH_MEASURE(0.001),#16679,
'DISTANCE_ACCURACY_VALUE',
'Maximum model space distance between geometric entities at asserted c
onnectivities');
#16614=UNCERTAINTY_MEASURE_WITH_UNIT(LENGTH_MEASURE(0.001),#16679,
'DISTANCE_ACCURACY_VALUE',
'Maximum model space distance between geometric entities at asserted c
onnectivities');
#16647=(
GEOMETRIC_REPRESENTATION_CONTEXT(3)
GLOBAL_UNCERTAINTY_ASSIGNED_CONTEXT((#16583))
GLOBAL_UNIT_ASSIGNED_CONTEXT((#16679,#16681,#16682))
REPRESENTATION_CONTEXT('','3D')
);
#16678=(
GEOMETRIC_REPRESENTATION_CONTEXT(3)
GLOBAL_UNCERTAINTY_ASSIGNED_CONTEXT((#16614))
GLOBAL_UNIT_ASSIGNED_CONTEXT((#16679,#16681,#16682))
REPRESENTATION_CONTEXT('','3D')
);
#16679=(
LENGTH_UNIT()
NAMED_UNIT(*)
SI_UNIT(.CENTI.,.METRE.)
);
#16681=(
NAMED_UNIT(*)
PLANE_ANGLE_UNIT()
SI_UNIT($,.RADIAN.)
);
#16682=(
NAMED_UNIT(*)
SI_UNIT($,.STERADIAN.)
SOLID_ANGLE_UNIT()
);
#16715=SHAPE_DEFINITION_REPRESENTATION(#16783,#16942);
#16783=PRODUCT_DEFINITION_SHAPE('',$,#17006);
#16942=SHAPE_REPRESENTATION('',(#10106),#16647);
#16973=PRODUCT_DEFINITION_CONTEXT('part definition',#17164,'design');
#17006=PRODUCT_DEFINITION('Pin keeper (1)','Pin keeper (1)',#17069,#16973);
#17069=PRODUCT_DEFINITION_FORMATION('',$,#17198);
#17164=APPLICATION_CONTEXT(
'Core Data for Automotive Mechanical Design Process');
#17165=PRODUCT_CONTEXT('part definition',#17164,'mechanical');
#17198=PRODUCT('Pin keeper (1)','Pin keeper (1)','Pin keeper (1)',(#17165));
#17285=COLOUR_RGB('Grey',0.48,0.52,0.57);
#17286=FILL_AREA_STYLE_COLOUR('',#17285);
#17287=FILL_AREA_STYLE('',(#17286));
#17288=SURFACE_STYLE_FILL_AREA(#17287);
#17289=SURFACE_SIDE_STYLE('',(#17288));
#17290=SURFACE_STYLE_USAGE(.BOTH.,#17289);
#17291=PRESENTATION_STYLE_ASSIGNMENT((#17290));
ENDSEC;
END-ISO-10303-21;
